ISO-10303-21;
HEADER;
/* Generated by software containing ST-Developer
 * from STEP Tools, Inc. (www.steptools.com) 
 */

FILE_DESCRIPTION(
/* description */ ('PAT-080'),
/* implementation_level */ '2;1');

FILE_NAME(
/* name */ 'Hex Nut - M8.step',
/* time_stamp */ '2026-10-29T20:13:47-07:00',
/* author */ (''),
/* organization */ (''),
/* preprocessor_version */ 'ST-DEVELOPER v20.2',
/* originating_system */ 'Autodesk Translation Framework v15.17.0.0',
/* authorisation */ '');

FILE_SCHEMA (('AUTOMOTIVE_DESIGN { 1 0 10303 214 3 1 1 }'));
ENDSEC;

DATA;
#10=MECHANICAL_DESIGN_GEOMETRIC_PRESENTATION_REPRESENTATION('',(#264),#6878);
#171=(
BOUNDED_CURVE()
B_SPLINE_CURVE(2,(#6724,#6725,#6726),.UNSPECIFIED.,.F.,.F.)
B_SPLINE_CURVE_WITH_KNOTS((3,3),(0.14973948338295,0.97160236658079),
 .UNSPECIFIED.)
CURVE()
GEOMETRIC_REPRESENTATION_ITEM()
RATIONAL_B_SPLINE_CURVE((1.07140024848292,1.23714644374248,1.07140024848292))
REPRESENTATION_ITEM('')
);
#172=(
BOUNDED_CURVE()
B_SPLINE_CURVE(2,(#6728,#6729,#6730),.UNSPECIFIED.,.F.,.F.)
B_SPLINE_CURVE_WITH_KNOTS((3,3),(0.14973948338295,0.971602366580789),
 .UNSPECIFIED.)
CURVE()
GEOMETRIC_REPRESENTATION_ITEM()
RATIONAL_B_SPLINE_CURVE((1.07140024848292,1.23714644374248,1.07140024848292))
REPRESENTATION_ITEM('')
);
#173=(
BOUNDED_CURVE()
B_SPLINE_CURVE(2,(#6735,#6736,#6737),.UNSPECIFIED.,.F.,.F.)
B_SPLINE_CURVE_WITH_KNOTS((3,3),(0.14973948338295,0.97160236658079),
 .UNSPECIFIED.)
CURVE()
GEOMETRIC_REPRESENTATION_ITEM()
RATIONAL_B_SPLINE_CURVE((1.07140024848292,1.23714644374248,1.07140024848292))
REPRESENTATION_ITEM('')
);
#174=(
BOUNDED_CURVE()
B_SPLINE_CURVE(2,(#6739,#6740,#6741),.UNSPECIFIED.,.F.,.F.)
B_SPLINE_CURVE_WITH_KNOTS((3,3),(0.14973948338295,0.97160236658079),
 .UNSPECIFIED.)
CURVE()
GEOMETRIC_REPRESENTATION_ITEM()
RATIONAL_B_SPLINE_CURVE((1.07140024848292,1.23714644374248,1.07140024848292))
REPRESENTATION_ITEM('')
);
#175=(
BOUNDED_CURVE()
B_SPLINE_CURVE(2,(#6743,#6744,#6745),.UNSPECIFIED.,.F.,.F.)
B_SPLINE_CURVE_WITH_KNOTS((3,3),(0.14973948338295,0.971602366580789),
 .UNSPECIFIED.)
CURVE()
GEOMETRIC_REPRESENTATION_ITEM()
RATIONAL_B_SPLINE_CURVE((1.07140024848292,1.23714644374248,1.07140024848292))
REPRESENTATION_ITEM('')
);
#176=(
BOUNDED_CURVE()
B_SPLINE_CURVE(2,(#6746,#6747,#6748),.UNSPECIFIED.,.F.,.F.)
B_SPLINE_CURVE_WITH_KNOTS((3,3),(0.14973948338295,0.97160236658079),
 .UNSPECIFIED.)
CURVE()
GEOMETRIC_REPRESENTATION_ITEM()
RATIONAL_B_SPLINE_CURVE((1.07140024848292,1.23714644374248,1.07140024848292))
REPRESENTATION_ITEM('')
);
#177=(
BOUNDED_CURVE()
B_SPLINE_CURVE(2,(#6755,#6756,#6757),.UNSPECIFIED.,.F.,.F.)
B_SPLINE_CURVE_WITH_KNOTS((3,3),(0.14973948338295,0.97160236658079),
 .UNSPECIFIED.)
CURVE()
GEOMETRIC_REPRESENTATION_ITEM()
RATIONAL_B_SPLINE_CURVE((1.07140024848292,1.23714644374248,1.07140024848292))
REPRESENTATION_ITEM('')
);
#178=(
BOUNDED_CURVE()
B_SPLINE_CURVE(2,(#6759,#6760,#6761),.UNSPECIFIED.,.F.,.F.)
B_SPLINE_CURVE_WITH_KNOTS((3,3),(0.14973948338295,0.97160236658079),
 .UNSPECIFIED.)
CURVE()
GEOMETRIC_REPRESENTATION_ITEM()
RATIONAL_B_SPLINE_CURVE((1.07140024848292,1.23714644374248,1.07140024848292))
REPRESENTATION_ITEM('')
);
#179=(
BOUNDED_CURVE()
B_SPLINE_CURVE(2,(#6763,#6764,#6765),.UNSPECIFIED.,.F.,.F.)
B_SPLINE_CURVE_WITH_KNOTS((3,3),(0.14973948338295,0.971602366580789),
 .UNSPECIFIED.)
CURVE()
GEOMETRIC_REPRESENTATION_ITEM()
RATIONAL_B_SPLINE_CURVE((1.07140024848292,1.23714644374248,1.07140024848292))
REPRESENTATION_ITEM('')
);
#180=(
BOUNDED_CURVE()
B_SPLINE_CURVE(2,(#6767,#6768,#6769),.UNSPECIFIED.,.F.,.F.)
B_SPLINE_CURVE_WITH_KNOTS((3,3),(0.14973948338295,0.97160236658079),
 .UNSPECIFIED.)
CURVE()
GEOMETRIC_REPRESENTATION_ITEM()
RATIONAL_B_SPLINE_CURVE((1.07140024848292,1.23714644374248,1.07140024848292))
REPRESENTATION_ITEM('')
);
#181=(
BOUNDED_CURVE()
B_SPLINE_CURVE(2,(#6771,#6772,#6773),.UNSPECIFIED.,.F.,.F.)
B_SPLINE_CURVE_WITH_KNOTS((3,3),(0.14973948338295,0.97160236658079),
 .UNSPECIFIED.)
CURVE()
GEOMETRIC_REPRESENTATION_ITEM()
RATIONAL_B_SPLINE_CURVE((1.07140024848292,1.23714644374248,1.07140024848292))
REPRESENTATION_ITEM('')
);
#182=(
BOUNDED_CURVE()
B_SPLINE_CURVE(2,(#6774,#6775,#6776),.UNSPECIFIED.,.F.,.F.)
B_SPLINE_CURVE_WITH_KNOTS((3,3),(0.14973948338295,0.971602366580789),
 .UNSPECIFIED.)
CURVE()
GEOMETRIC_REPRESENTATION_ITEM()
RATIONAL_B_SPLINE_CURVE((1.07140024848292,1.23714644374248,1.07140024848292))
REPRESENTATION_ITEM('')
);
#200=CONICAL_SURFACE('',#4479,0.734027674973257,1.0471975511966);
#201=CONICAL_SURFACE('',#4481,0.734027674973257,1.0471975511966);
#226=SHAPE_REPRESENTATION_RELATIONSHIP('SRR','None',#6982,#245);
#245=ADVANCED_BREP_SHAPE_REPRESENTATION('',(#280),#6877);
#264=STYLED_ITEM('',(#7136),#280);
#280=MANIFOLD_SOLID_BREP('Body1',#3883);
#355=FACE_BOUND('',#1025,.T.);
#356=FACE_BOUND('',#1027,.T.);
#492=PLANE('',#4483);
#493=PLANE('',#4484);
#494=PLANE('',#4485);
#495=PLANE('',#4489);
#496=PLANE('',#4490);
#497=PLANE('',#4491);
#498=PLANE('',#4492);
#499=PLANE('',#4493);
#715=FACE_OUTER_BOUND('',#1015,.T.);
#716=FACE_OUTER_BOUND('',#1016,.T.);
#717=FACE_OUTER_BOUND('',#1017,.T.);
#718=FACE_OUTER_BOUND('',#1018,.T.);
#719=FACE_OUTER_BOUND('',#1019,.T.);
#720=FACE_OUTER_BOUND('',#1020,.T.);
#721=FACE_OUTER_BOUND('',#1021,.T.);
#722=FACE_OUTER_BOUND('',#1022,.T.);
#723=FACE_OUTER_BOUND('',#1023,.T.);
#724=FACE_OUTER_BOUND('',#1024,.T.);
#725=FACE_OUTER_BOUND('',#1026,.T.);
#1015=EDGE_LOOP('',(#3520,#3521,#3522,#3523,#3524,#3525,#3526,#3527,#3528));
#1016=EDGE_LOOP('',(#3529,#3530,#3531,#3532,#3533,#3534,#3535,#3536,#3537));
#1017=EDGE_LOOP('',(#3538,#3539,#3540,#3541));
#1018=EDGE_LOOP('',(#3542,#3543,#3544,#3545));
#1019=EDGE_LOOP('',(#3546,#3547,#3548,#3549));
#1020=EDGE_LOOP('',(#3550,#3551,#3552,#3553));
#1021=EDGE_LOOP('',(#3554,#3555,#3556,#3557));
#1022=EDGE_LOOP('',(#3558,#3559,#3560,#3561));
#1023=EDGE_LOOP('',(#3562,#3563,#3564,#3565));
#1024=EDGE_LOOP('',(#3566));
#1025=EDGE_LOOP('',(#3567));
#1026=EDGE_LOOP('',(#3568));
#1027=EDGE_LOOP('',(#3569));
#1334=LINE('',#6732,#1649);
#1335=LINE('',#6753,#1650);
#1336=LINE('',#6778,#1651);
#1337=LINE('',#6779,#1652);
#1338=LINE('',#6781,#1653);
#1339=LINE('',#6783,#1654);
#1340=LINE('',#6788,#1655);
#1341=LINE('',#6791,#1656);
#1342=LINE('',#6793,#1657);
#1649=VECTOR('',#5612,0.734027674973257);
#1650=VECTOR('',#5619,0.734027674973257);
#1651=VECTOR('',#5622,1.);
#1652=VECTOR('',#5623,1.);
#1653=VECTOR('',#5626,1.);
#1654=VECTOR('',#5629,1.);
#1655=VECTOR('',#5634,0.4);
#1656=VECTOR('',#5639,1.);
#1657=VECTOR('',#5642,1.);
#1806=CIRCLE('',#4480,0.6175);
#1807=CIRCLE('',#4482,0.6175);
#1808=CIRCLE('',#4487,0.338975);
#1809=CIRCLE('',#4488,0.338975);
#2111=VERTEX_POINT('',#6722);
#2112=VERTEX_POINT('',#6723);
#2113=VERTEX_POINT('',#6727);
#2114=VERTEX_POINT('',#6731);
#2115=VERTEX_POINT('',#6734);
#2116=VERTEX_POINT('',#6738);
#2117=VERTEX_POINT('',#6742);
#2118=VERTEX_POINT('',#6750);
#2119=VERTEX_POINT('',#6752);
#2120=VERTEX_POINT('',#6754);
#2121=VERTEX_POINT('',#6758);
#2122=VERTEX_POINT('',#6762);
#2123=VERTEX_POINT('',#6766);
#2124=VERTEX_POINT('',#6770);
#2125=VERTEX_POINT('',#6785);
#2126=VERTEX_POINT('',#6787);
#2583=EDGE_CURVE('',#2111,#2112,#171,.T.);
#2584=EDGE_CURVE('',#2113,#2111,#172,.T.);
#2585=EDGE_CURVE('',#2113,#2114,#1334,.T.);
#2586=EDGE_CURVE('',#2114,#2114,#1806,.T.);
#2587=EDGE_CURVE('',#2115,#2113,#173,.T.);
#2588=EDGE_CURVE('',#2116,#2115,#174,.T.);
#2589=EDGE_CURVE('',#2117,#2116,#175,.T.);
#2590=EDGE_CURVE('',#2112,#2117,#176,.T.);
#2591=EDGE_CURVE('',#2118,#2118,#1807,.T.);
#2592=EDGE_CURVE('',#2118,#2119,#1335,.T.);
#2593=EDGE_CURVE('',#2120,#2119,#177,.T.);
#2594=EDGE_CURVE('',#2121,#2120,#178,.T.);
#2595=EDGE_CURVE('',#2122,#2121,#179,.T.);
#2596=EDGE_CURVE('',#2123,#2122,#180,.T.);
#2597=EDGE_CURVE('',#2124,#2123,#181,.T.);
#2598=EDGE_CURVE('',#2119,#2124,#182,.T.);
#2599=EDGE_CURVE('',#2115,#2124,#1336,.T.);
#2600=EDGE_CURVE('',#2116,#2123,#1337,.T.);
#2601=EDGE_CURVE('',#2113,#2119,#1338,.T.);
#2602=EDGE_CURVE('',#2111,#2120,#1339,.T.);
#2603=EDGE_CURVE('',#2125,#2125,#1808,.F.);
#2604=EDGE_CURVE('',#2125,#2126,#1340,.T.);
#2605=EDGE_CURVE('',#2126,#2126,#1809,.F.);
#2606=EDGE_CURVE('',#2112,#2121,#1341,.T.);
#2607=EDGE_CURVE('',#2117,#2122,#1342,.T.);
#3520=ORIENTED_EDGE('',*,*,#2583,.F.);
#3521=ORIENTED_EDGE('',*,*,#2584,.F.);
#3522=ORIENTED_EDGE('',*,*,#2585,.T.);
#3523=ORIENTED_EDGE('',*,*,#2586,.F.);
#3524=ORIENTED_EDGE('',*,*,#2585,.F.);
#3525=ORIENTED_EDGE('',*,*,#2587,.F.);
#3526=ORIENTED_EDGE('',*,*,#2588,.F.);
#3527=ORIENTED_EDGE('',*,*,#2589,.F.);
#3528=ORIENTED_EDGE('',*,*,#2590,.F.);
#3529=ORIENTED_EDGE('',*,*,#2591,.F.);
#3530=ORIENTED_EDGE('',*,*,#2592,.T.);
#3531=ORIENTED_EDGE('',*,*,#2593,.F.);
#3532=ORIENTED_EDGE('',*,*,#2594,.F.);
#3533=ORIENTED_EDGE('',*,*,#2595,.F.);
#3534=ORIENTED_EDGE('',*,*,#2596,.F.);
#3535=ORIENTED_EDGE('',*,*,#2597,.F.);
#3536=ORIENTED_EDGE('',*,*,#2598,.F.);
#3537=ORIENTED_EDGE('',*,*,#2592,.F.);
#3538=ORIENTED_EDGE('',*,*,#2588,.T.);
#3539=ORIENTED_EDGE('',*,*,#2599,.T.);
#3540=ORIENTED_EDGE('',*,*,#2597,.T.);
#3541=ORIENTED_EDGE('',*,*,#2600,.F.);
#3542=ORIENTED_EDGE('',*,*,#2587,.T.);
#3543=ORIENTED_EDGE('',*,*,#2601,.T.);
#3544=ORIENTED_EDGE('',*,*,#2598,.T.);
#3545=ORIENTED_EDGE('',*,*,#2599,.F.);
#3546=ORIENTED_EDGE('',*,*,#2584,.T.);
#3547=ORIENTED_EDGE('',*,*,#2602,.T.);
#3548=ORIENTED_EDGE('',*,*,#2593,.T.);
#3549=ORIENTED_EDGE('',*,*,#2601,.F.);
#3550=ORIENTED_EDGE('',*,*,#2603,.F.);
#3551=ORIENTED_EDGE('',*,*,#2604,.T.);
#3552=ORIENTED_EDGE('',*,*,#2605,.T.);
#3553=ORIENTED_EDGE('',*,*,#2604,.F.);
#3554=ORIENTED_EDGE('',*,*,#2583,.T.);
#3555=ORIENTED_EDGE('',*,*,#2606,.T.);
#3556=ORIENTED_EDGE('',*,*,#2594,.T.);
#3557=ORIENTED_EDGE('',*,*,#2602,.F.);
#3558=ORIENTED_EDGE('',*,*,#2589,.T.);
#3559=ORIENTED_EDGE('',*,*,#2600,.T.);
#3560=ORIENTED_EDGE('',*,*,#2596,.T.);
#3561=ORIENTED_EDGE('',*,*,#2607,.F.);
#3562=ORIENTED_EDGE('',*,*,#2590,.T.);
#3563=ORIENTED_EDGE('',*,*,#2607,.T.);
#3564=ORIENTED_EDGE('',*,*,#2595,.T.);
#3565=ORIENTED_EDGE('',*,*,#2606,.F.);
#3566=ORIENTED_EDGE('',*,*,#2591,.T.);
#3567=ORIENTED_EDGE('',*,*,#2603,.T.);
#3568=ORIENTED_EDGE('',*,*,#2586,.T.);
#3569=ORIENTED_EDGE('',*,*,#2605,.F.);
#3635=CYLINDRICAL_SURFACE('',#4486,0.338975);
#3851=ADVANCED_FACE('',(#715),#200,.T.);
#3852=ADVANCED_FACE('',(#716),#201,.T.);
#3853=ADVANCED_FACE('',(#717),#492,.T.);
#3854=ADVANCED_FACE('',(#718),#493,.T.);
#3855=ADVANCED_FACE('',(#719),#494,.T.);
#3856=ADVANCED_FACE('',(#720),#3635,.F.);
#3857=ADVANCED_FACE('',(#721),#495,.T.);
#3858=ADVANCED_FACE('',(#722),#496,.T.);
#3859=ADVANCED_FACE('',(#723),#497,.T.);
#3860=ADVANCED_FACE('',(#724,#355),#498,.T.);
#3861=ADVANCED_FACE('',(#725,#356),#499,.F.);
#3883=CLOSED_SHELL('',(#3851,#3852,#3853,#3854,#3855,#3856,#3857,#3858,
#3859,#3860,#3861));
#4478=AXIS2_PLACEMENT_3D('',#6720,#5608,#5609);
#4479=AXIS2_PLACEMENT_3D('',#6721,#5610,#5611);
#4480=AXIS2_PLACEMENT_3D('',#6733,#5613,#5614);
#4481=AXIS2_PLACEMENT_3D('',#6749,#5615,#5616);
#4482=AXIS2_PLACEMENT_3D('',#6751,#5617,#5618);
#4483=AXIS2_PLACEMENT_3D('',#6777,#5620,#5621);
#4484=AXIS2_PLACEMENT_3D('',#6780,#5624,#5625);
#4485=AXIS2_PLACEMENT_3D('',#6782,#5627,#5628);
#4486=AXIS2_PLACEMENT_3D('',#6784,#5630,#5631);
#4487=AXIS2_PLACEMENT_3D('',#6786,#5632,#5633);
#4488=AXIS2_PLACEMENT_3D('',#6789,#5635,#5636);
#4489=AXIS2_PLACEMENT_3D('',#6790,#5637,#5638);
#4490=AXIS2_PLACEMENT_3D('',#6792,#5640,#5641);
#4491=AXIS2_PLACEMENT_3D('',#6794,#5643,#5644);
#4492=AXIS2_PLACEMENT_3D('',#6795,#5645,#5646);
#4493=AXIS2_PLACEMENT_3D('',#6796,#5647,#5648);
#5608=DIRECTION('axis',(0.,0.,1.));
#5609=DIRECTION('refdir',(1.,0.,0.));
#5610=DIRECTION('center_axis',(0.,1.,0.));
#5611=DIRECTION('ref_axis',(1.,0.,0.));
#5612=DIRECTION('',(0.866025403784439,-0.5,1.06057523872491E-16));
#5613=DIRECTION('center_axis',(0.,-1.,0.));
#5614=DIRECTION('ref_axis',(1.,0.,0.));
#5615=DIRECTION('center_axis',(0.,-1.,0.));
#5616=DIRECTION('ref_axis',(1.,0.,0.));
#5617=DIRECTION('center_axis',(0.,1.,0.));
#5618=DIRECTION('ref_axis',(1.,0.,0.));
#5619=DIRECTION('',(-0.866025403784439,-0.5,-1.06057523872491E-16));
#5620=DIRECTION('center_axis',(1.4792020664489E-16,0.,-1.));
#5621=DIRECTION('ref_axis',(-1.,0.,-1.4792020664489E-16));
#5622=DIRECTION('',(0.,1.,0.));
#5623=DIRECTION('',(0.,1.,0.));
#5624=DIRECTION('center_axis',(-0.866025403784439,0.,-0.5));
#5625=DIRECTION('ref_axis',(-0.5,0.,0.866025403784439));
#5626=DIRECTION('',(0.,1.,0.));
#5627=DIRECTION('center_axis',(-0.866025403784439,0.,0.5));
#5628=DIRECTION('ref_axis',(0.5,0.,0.866025403784439));
#5629=DIRECTION('',(0.,1.,0.));
#5630=DIRECTION('center_axis',(0.,1.,0.));
#5631=DIRECTION('ref_axis',(1.,0.,0.));
#5632=DIRECTION('center_axis',(0.,1.,0.));
#5633=DIRECTION('ref_axis',(1.,0.,0.));
#5634=DIRECTION('',(0.,-1.,0.));
#5635=DIRECTION('center_axis',(0.,1.,0.));
#5636=DIRECTION('ref_axis',(1.,0.,0.));
#5637=DIRECTION('center_axis',(-2.95840413289779E-16,0.,1.));
#5638=DIRECTION('ref_axis',(1.,0.,2.95840413289779E-16));
#5639=DIRECTION('',(0.,1.,0.));
#5640=DIRECTION('center_axis',(0.866025403784439,0.,-0.5));
#5641=DIRECTION('ref_axis',(-0.5,0.,-0.866025403784439));
#5642=DIRECTION('',(0.,1.,0.));
#5643=DIRECTION('center_axis',(0.866025403784439,0.,0.5));
#5644=DIRECTION('ref_axis',(0.5,0.,-0.866025403784439));
#5645=DIRECTION('center_axis',(0.,1.,0.));
#5646=DIRECTION('ref_axis',(1.,0.,0.));
#5647=DIRECTION('center_axis',(0.,1.,0.));
#5648=DIRECTION('ref_axis',(1.,0.,0.));
#6720=CARTESIAN_POINT('',(0.,0.,0.));
#6721=CARTESIAN_POINT('Origin',(0.,0.067277284513851,0.));
#6722=CARTESIAN_POINT('',(-0.375277674973257,0.0768195421087395,0.65));
#6723=CARTESIAN_POINT('',(0.375277674973257,0.0768195421087395,0.65));
#6724=CARTESIAN_POINT('Ctrl Pts',(-0.375277674973257,0.0768195421087395,
0.65));
#6725=CARTESIAN_POINT('Ctrl Pts',(1.66533453693773E-13,-0.0315137912242439,
0.65));
#6726=CARTESIAN_POINT('Ctrl Pts',(0.375277674973257,0.0768195421087394,
0.65));
#6727=CARTESIAN_POINT('',(-0.750555349946514,0.0768195421087394,-9.19165206894919E-17));
#6728=CARTESIAN_POINT('Ctrl Pts',(-0.750555349946514,0.0768195421087394,
-9.19165206894919E-17));
#6729=CARTESIAN_POINT('Ctrl Pts',(-0.562916512459802,-0.0315137912242434,
0.325000000000144));
#6730=CARTESIAN_POINT('Ctrl Pts',(-0.375277674973257,0.0768195421087395,
0.65));
#6731=CARTESIAN_POINT('',(-0.6175,-2.77555756156289E-17,-7.5621939847349E-17));
#6732=CARTESIAN_POINT('',(-0.734027674973257,0.067277284513851,-8.98924642641573E-17));
#6733=CARTESIAN_POINT('Origin',(0.,0.,0.));
#6734=CARTESIAN_POINT('',(-0.375277674973257,0.0768195421087395,-0.65));
#6735=CARTESIAN_POINT('Ctrl Pts',(-0.375277674973257,0.0768195421087395,
-0.65));
#6736=CARTESIAN_POINT('Ctrl Pts',(-0.562916512459968,-0.0315137912242437,
-0.324999999999856));
#6737=CARTESIAN_POINT('Ctrl Pts',(-0.750555349946514,0.0768195421087395,
-9.19165206894919E-17));
#6738=CARTESIAN_POINT('',(0.375277674973257,0.0768195421087395,-0.65));
#6739=CARTESIAN_POINT('Ctrl Pts',(0.375277674973257,0.0768195421087395,
-0.65));
#6740=CARTESIAN_POINT('Ctrl Pts',(-1.66144875635155E-13,-0.0315137912242437,
-0.65));
#6741=CARTESIAN_POINT('Ctrl Pts',(-0.375277674973257,0.0768195421087395,
-0.65));
#6742=CARTESIAN_POINT('',(0.750555349946514,0.0768195421087394,0.));
#6743=CARTESIAN_POINT('Ctrl Pts',(0.750555349946514,0.0768195421087394,
0.));
#6744=CARTESIAN_POINT('Ctrl Pts',(0.562916512459802,-0.0315137912242436,
-0.325000000000144));
#6745=CARTESIAN_POINT('Ctrl Pts',(0.375277674973257,0.0768195421087395,
-0.65));
#6746=CARTESIAN_POINT('Ctrl Pts',(0.375277674973257,0.0768195421087394,
0.65));
#6747=CARTESIAN_POINT('Ctrl Pts',(0.562916512459968,-0.0315137912242439,
0.324999999999856));
#6748=CARTESIAN_POINT('Ctrl Pts',(0.750555349946514,0.0768195421087394,
0.));
#6749=CARTESIAN_POINT('Origin',(0.,0.612722715486149,0.));
#6750=CARTESIAN_POINT('',(-0.6175,0.68,-7.5621939847349E-17));
#6751=CARTESIAN_POINT('Origin',(0.,0.68,0.));
#6752=CARTESIAN_POINT('',(-0.750555349946514,0.603180457891261,-9.19165206894919E-17));
#6753=CARTESIAN_POINT('',(-0.734027674973257,0.612722715486149,-8.98924642641573E-17));
#6754=CARTESIAN_POINT('',(-0.375277674973257,0.603180457891261,0.65));
#6755=CARTESIAN_POINT('Ctrl Pts',(-0.375277674973257,0.603180457891261,
0.65));
#6756=CARTESIAN_POINT('Ctrl Pts',(-0.562916512459968,0.711513791224243,
0.324999999999856));
#6757=CARTESIAN_POINT('Ctrl Pts',(-0.750555349946514,0.603180457891261,
-9.19165206894919E-17));
#6758=CARTESIAN_POINT('',(0.375277674973257,0.603180457891261,0.65));
#6759=CARTESIAN_POINT('Ctrl Pts',(0.375277674973257,0.603180457891261,0.65));
#6760=CARTESIAN_POINT('Ctrl Pts',(-1.66755498298699E-13,0.711513791224244,
0.65));
#6761=CARTESIAN_POINT('Ctrl Pts',(-0.375277674973257,0.603180457891261,
0.65));
#6762=CARTESIAN_POINT('',(0.750555349946514,0.603180457891261,0.));
#6763=CARTESIAN_POINT('Ctrl Pts',(0.750555349946514,0.603180457891261,0.));
#6764=CARTESIAN_POINT('Ctrl Pts',(0.562916512459802,0.711513791224244,0.325000000000144));
#6765=CARTESIAN_POINT('Ctrl Pts',(0.375277674973257,0.603180457891261,0.65));
#6766=CARTESIAN_POINT('',(0.375277674973257,0.603180457891261,-0.65));
#6767=CARTESIAN_POINT('Ctrl Pts',(0.375277674973257,0.603180457891261,-0.65));
#6768=CARTESIAN_POINT('Ctrl Pts',(0.562916512459969,0.711513791224244,-0.324999999999856));
#6769=CARTESIAN_POINT('Ctrl Pts',(0.750555349946514,0.603180457891261,0.));
#6770=CARTESIAN_POINT('',(-0.375277674973257,0.603180457891261,-0.65));
#6771=CARTESIAN_POINT('Ctrl Pts',(-0.375277674973257,0.603180457891261,
-0.65));
#6772=CARTESIAN_POINT('Ctrl Pts',(1.66422431391311E-13,0.711513791224244,
-0.65));
#6773=CARTESIAN_POINT('Ctrl Pts',(0.375277674973257,0.603180457891261,-0.65));
#6774=CARTESIAN_POINT('Ctrl Pts',(-0.750555349946514,0.603180457891261,
-9.19165206894919E-17));
#6775=CARTESIAN_POINT('Ctrl Pts',(-0.562916512459802,0.711513791224244,
-0.325000000000144));
#6776=CARTESIAN_POINT('Ctrl Pts',(-0.375277674973257,0.603180457891261,
-0.65));
#6777=CARTESIAN_POINT('Origin',(0.375277674973257,0.,-0.65));
#6778=CARTESIAN_POINT('',(-0.375277674973257,0.,-0.65));
#6779=CARTESIAN_POINT('',(0.375277674973257,0.,-0.65));
#6780=CARTESIAN_POINT('Origin',(-0.375277674973257,0.,-0.65));
#6781=CARTESIAN_POINT('',(-0.750555349946514,0.,-9.19165206894919E-17));
#6782=CARTESIAN_POINT('Origin',(-0.750555349946514,0.,-9.19165206894919E-17));
#6783=CARTESIAN_POINT('',(-0.375277674973257,0.,0.65));
#6784=CARTESIAN_POINT('Origin',(0.,0.,0.));
#6785=CARTESIAN_POINT('',(-0.338975,0.68,4.15124648740974E-17));
#6786=CARTESIAN_POINT('Origin',(0.,0.68,0.));
#6787=CARTESIAN_POINT('',(-0.338975,0.,4.15124648740974E-17));
#6788=CARTESIAN_POINT('',(-0.338975,0.,4.15124648740974E-17));
#6789=CARTESIAN_POINT('Origin',(0.,0.,0.));
#6790=CARTESIAN_POINT('Origin',(-0.375277674973257,0.,0.65));
#6791=CARTESIAN_POINT('',(0.375277674973257,0.,0.65));
#6792=CARTESIAN_POINT('Origin',(0.750555349946514,0.,0.));
#6793=CARTESIAN_POINT('',(0.750555349946514,0.,0.));
#6794=CARTESIAN_POINT('Origin',(0.375277674973257,0.,0.65));
#6795=CARTESIAN_POINT('Origin',(0.,0.68,-1.11022302462516E-16));
#6796=CARTESIAN_POINT('Origin',(0.,0.,-1.11022302462516E-16));
#6856=UNCERTAINTY_MEASURE_WITH_UNIT(LENGTH_MEASURE(0.001),#6879,
'DISTANCE_ACCURACY_VALUE',
'Maximum model space distance between geometric entities at asserted c
onnectivities');
#6857=UNCERTAINTY_MEASURE_WITH_UNIT(LENGTH_MEASURE(0.001),#6879,
'DISTANCE_ACCURACY_VALUE',
'Maximum model space distance between geometric entities at asserted c
onnectivities');
#6877=(
GEOMETRIC_REPRESENTATION_CONTEXT(3)
GLOBAL_UNCERTAINTY_ASSIGNED_CONTEXT((#6856))
GLOBAL_UNIT_ASSIGNED_CONTEXT((#6879,#6881,#6882))
REPRESENTATION_CONTEXT('','3D')
);
#6878=(
GEOMETRIC_REPRESENTATION_CONTEXT(3)
GLOBAL_UNCERTAINTY_ASSIGNED_CONTEXT((#6857))
GLOBAL_UNIT_ASSIGNED_CONTEXT((#6879,#6881,#6882))
REPRESENTATION_CONTEXT('','3D')
);
#6879=(
LENGTH_UNIT()
NAMED_UNIT(*)
SI_UNIT(.CENTI.,.METRE.)
);
#6881=(
NAMED_UNIT(*)
PLANE_ANGLE_UNIT()
SI_UNIT($,.RADIAN.)
);
#6882=(
NAMED_UNIT(*)
SI_UNIT($,.STERADIAN.)
SOLID_ANGLE_UNIT()
);
#6902=SHAPE_DEFINITION_REPRESENTATION(#6922,#6982);
#6922=PRODUCT_DEFINITION_SHAPE('',$,#7003);
#6982=SHAPE_REPRESENTATION('',(#4478),#6877);
#6983=PRODUCT_DEFINITION_CONTEXT('part definition',#7045,'design');
#7003=PRODUCT_DEFINITION('Hex Nut - M8','Hex Nut - M8',#7023,
#6983);
#7023=PRODUCT_DEFINITION_FORMATION('',$,#7066);
#7045=APPLICATION_CONTEXT(
'Core Data for Automotive Mechanical Design Process');
#7046=PRODUCT_CONTEXT('part definition',#7045,'mechanical');
#7066=PRODUCT('Hex Nut - M8','Hex Nut - M8','Hex Nut - M8',
(#7046));
#7130=COLOUR_RGB('Black',0.12,0.14,0.17);
#7131=FILL_AREA_STYLE_COLOUR('',#7130);
#7132=FILL_AREA_STYLE('',(#7131));
#7133=SURFACE_STYLE_FILL_AREA(#7132);
#7134=SURFACE_SIDE_STYLE('',(#7133));
#7135=SURFACE_STYLE_USAGE(.BOTH.,#7134);
#7136=PRESENTATION_STYLE_ASSIGNMENT((#7135));
ENDSEC;
END-ISO-10303-21;
